ISO-10303-21;
HEADER;
FILE_DESCRIPTION (('STEP AP214'),
    '1' );
FILE_NAME ('Screw 7.step',
    '2026-10-26T17:37:43',
    ( '' ),
    ( '' ),
    'SwSTEP 2.0',
    'SolidWorks 2024',
    '' );
FILE_SCHEMA (( 'AUTOMOTIVE_DESIGN' ));
ENDSEC;

DATA;
#12=CARTESIAN_POINT ( 'NONE',  ( 17.78000000000000114, -3579.494999999999891, 2239.009999999999764 ) ) ;
#55=EDGE_CURVE ( 'NONE', #4791, #12834, #15371, .T. ) ;
#129=EDGE_LOOP ( 'NONE', ( #9920, #914 ) ) ;
#172=CARTESIAN_POINT ( 'NONE',  ( 10.36831320293797276, -3578.148799999986750, 2239.391000000000076 ) ) ;
#173=PLANE ( 'NONE',  #10602 ) ;
#224=CARTESIAN_POINT ( 'NONE',  ( 12.69999999999999929, -3579.494999999999891, 2270.760000000000218 ) ) ;
#271=ORIENTED_EDGE ( 'NONE', *, *, #4706, .F. ) ;
#323=DIRECTION ( 'NONE',  ( 0.000000000000000000, -1.000000000000000000, 0.000000000000000000 ) ) ;
#385=EDGE_LOOP ( 'NONE', ( #5161, #4058, #19864, #16959, #15147, #3031 ) ) ;
#450=LINE ( 'NONE', #16612, #19312 ) ;
#536=SHAPE_REPRESENTATION ( 'Screw 7', ( #5611 ), #5641 ) ;
#587=ORIENTED_EDGE ( 'NONE', *, *, #13824, .T. ) ;
#627=DIRECTION ( 'NONE',  ( 0.000000000000000000, 0.000000000000000000, 1.000000000000000000 ) ) ;
#706=EDGE_CURVE ( 'NONE', #19558, #12468, #18680, .T. ) ;
#732=CARTESIAN_POINT ( 'NONE',  ( 18.16100000000000136, -3579.494999999999891, 2244.978999999999814 ) ) ;
#748=ORIENTED_EDGE ( 'NONE', *, *, #10145, .F. ) ;
#894=VERTEX_POINT ( 'NONE', #19852 ) ;
#914=ORIENTED_EDGE ( 'NONE', *, *, #14134, .T. ) ;
#960=AXIS2_PLACEMENT_3D ( 'NONE', #3818, #7804, #11891 ) ;
#981=ORIENTED_EDGE ( 'NONE', *, *, #2428, .F. ) ;
#990=DIRECTION ( 'NONE',  ( 0.000000000000000000, -1.000000000000000000, 0.000000000000000000 ) ) ;
#991=CARTESIAN_POINT ( 'NONE',  ( 12.70000000002640839, -3576.802599999929498, 2239.391000000000076 ) ) ;
#1035=CYLINDRICAL_SURFACE ( 'NONE', #23027, 0.3809999999999993947 ) ;
#1098=EDGE_LOOP ( 'NONE', ( #981, #7188, #17231, #14230, #4142, #11385 ) ) ;
#1123=CARTESIAN_POINT ( 'NONE',  ( 10.36831320285999958, -3580.841199999999844, 2242.820000000000164 ) ) ;
#1141=DIRECTION ( 'NONE',  ( -2.324635735433000053E-14, 0.000000000000000000, -1.000000000000000000 ) ) ;
#1162=ORIENTED_EDGE ( 'NONE', *, *, #20568, .T. ) ;
#1193=DIRECTION ( 'NONE',  ( 0.000000000000000000, 0.000000000000000000, -1.000000000000000000 ) ) ;
#1217=DIRECTION ( 'NONE',  ( 4.097771990502999700E-13, -2.590196616219000170E-13, -1.000000000000000000 ) ) ;
#1240=DIRECTION ( 'NONE',  ( -0.8660254037840939834, -0.5000000000005969669, 0.000000000000000000 ) ) ;
#1266=CARTESIAN_POINT ( 'NONE',  ( 15.03168679716000078, -3575.456400000000031, 2242.820000000000164 ) ) ;
#1311=DIRECTION ( 'NONE',  ( 5.572969907074833723E-14, -1.000000000000000000, 0.000000000000000000 ) ) ;
#1335=ORIENTED_EDGE ( 'NONE', *, *, #23003, .T. ) ;
#1364=EDGE_CURVE ( 'NONE', #12078, #18476, #5648, .T. ) ;
#1408=CARTESIAN_POINT ( 'NONE',  ( 7.619999999999999218, -3579.494999999999891, 2239.391000000000076 ) ) ;
#1425=EDGE_LOOP ( 'NONE', ( #2306, #2869, #6704, #11786, #21167, #11479 ) ) ;
#1474=ORIENTED_EDGE ( 'NONE', *, *, #13164, .F. ) ;
#1476=LINE ( 'NONE', #12271, #6217 ) ;
#1536=ORIENTED_EDGE ( 'NONE', *, *, #19257, .F. ) ;
#1602=EDGE_LOOP ( 'NONE', ( #22191, #17975, #17577, #13431 ) ) ;
#1748=DIRECTION ( 'NONE',  ( -3.627287058276000189E-13, 1.295098308114999897E-13, 1.000000000000000000 ) ) ;
#1749=VECTOR ( 'NONE', #4374, 1000.000000000000000 ) ;
#1768=CARTESIAN_POINT ( 'NONE',  ( 15.03168679716000078, -3578.148799999999937, 2239.391000000000076 ) ) ;
#1811=DIRECTION ( 'NONE',  ( 1.000000000000000000, 5.432398939370943590E-28, -2.324635735433000369E-14 ) ) ;
#1843=EDGE_LOOP ( 'NONE', ( #9140, #587, #1474, #10656 ) ) ;
#1848=TOROIDAL_SURFACE ( 'NONE', #5970, 1.905000000000000027, 1.270000000000000018 ) ;
#1894=DIRECTION ( 'NONE',  ( -2.324635735433000053E-14, 2.336881798971000105E-14, -1.000000000000000000 ) ) ;
#1896=PLANE ( 'NONE',  #19362 ) ;
#1941=VECTOR ( 'NONE', #18173, 1000.000000000000000 ) ;
#1946=CYLINDRICAL_SURFACE ( 'NONE', #20025, 3.175000000000149925 ) ;
#1980=ORIENTED_EDGE ( 'NONE', *, *, #3904, .T. ) ;
#2074=AXIS2_PLACEMENT_3D ( 'NONE', #5740, #11334, #11119 ) ;
#2085=FACE_OUTER_BOUND ( 'NONE', #19880, .T. ) ;
#2093=ADVANCED_FACE ( 'NONE', ( #15324 ), #10394, .T. ) ;
#2138=EDGE_CURVE ( 'NONE', #3607, #17982, #10040, .T. ) ;
#2177=LINE ( 'NONE', #9322, #8912 ) ;
#2195=FACE_OUTER_BOUND ( 'NONE', #129, .T. ) ;
#2210=LINE ( 'NONE', #19905, #5083 ) ;
#2251=AXIS2_PLACEMENT_3D ( 'NONE', #20840, #15569, #6552 ) ;
#2257=( GEOMETRIC_REPRESENTATION_CONTEXT ( 3 ) GLOBAL_UNCERTAINTY_ASSIGNED_CONTEXT ( ( #16741 ) ) GLOBAL_UNIT_ASSIGNED_CONTEXT ( ( #21126, #3419, #23094 ) ) REPRESENTATION_CONTEXT ( 'NONE', 'WORKASPACE' ) );
#2296=EDGE_LOOP ( 'NONE', ( #15009, #19833, #11316, #19725 ) ) ;
#2303=LINE ( 'NONE', #8352, #7231 ) ;
#2306=ORIENTED_EDGE ( 'NONE', *, *, #7142, .T. ) ;
#2342=CARTESIAN_POINT ( 'NONE',  ( 15.41268679715999923, -3577.928829547000078, 2239.009999999999764 ) ) ;
#2347=ADVANCED_FACE ( 'NONE', ( #4287, #2195 ), #22085, .F. ) ;
#2359=CIRCLE ( 'NONE', #18061, 5.080000000000000071 ) ;
#2412=ADVANCED_FACE ( 'NONE', ( #12969 ), #20227, .T. ) ;
#2428=EDGE_CURVE ( 'NONE', #5562, #12269, #2303, .T. ) ;
#2472=AXIS2_PLACEMENT_3D ( 'NONE', #1266, #12053, #7254 ) ;
#2506=CARTESIAN_POINT ( 'NONE',  ( 12.70000000005999929, -3576.802599999999984, 2239.391000000000076 ) ) ;
#2550=DIRECTION ( 'NONE',  ( 0.000000000000000000, 0.000000000000000000, -1.000000000000000000 ) ) ;
#2554=EDGE_CURVE ( 'NONE', #894, #12269, #4824, .T. ) ;
#2578=CIRCLE ( 'NONE', #20535, 1.904999999999823501 ) ;
#2588=CARTESIAN_POINT ( 'NONE',  ( 12.69999999999999929, -3574.034000000000106, 2244.978999999999814 ) ) ;
#2606=CARTESIAN_POINT ( 'NONE',  ( 0.000000000000000000, 0.000000000000000000, 0.000000000000000000 ) ) ;
#2623=DIRECTION ( 'NONE',  ( 0.000000000000000000, 0.000000000000000000, -1.000000000000000000 ) ) ;
#2630=CARTESIAN_POINT ( 'NONE',  ( 12.69999999999999929, -3579.494999999999891, 2239.009999999999764 ) ) ;
#2656=ADVANCED_FACE ( 'NONE', ( #16529 ), #4113, .T. ) ;
#2660=VECTOR ( 'NONE', #13310, 1000.000000000000000 ) ;
#2689=EDGE_LOOP ( 'NONE', ( #21721, #1162, #10236, #6621, #22216 ) ) ;
#2718=DIRECTION ( 'NONE',  ( 0.000000000000000000, -1.000000000000000000, 0.000000000000000000 ) ) ;
#2719=DIRECTION ( 'NONE',  ( 0.000000000000000000, 2.336881798971000105E-14, -1.000000000000000000 ) ) ;
#2747=ORIENTED_EDGE ( 'NONE', *, *, #14005, .F. ) ;
#2750=VERTEX_POINT ( 'NONE', #9163 ) ;
#2837=CARTESIAN_POINT ( 'NONE',  ( 12.69999999999999929, -3581.400000000000091, 2270.760000000000218 ) ) ;
#2846=DIRECTION ( 'NONE',  ( 1.224646799141920914E-16, -1.000000000000000000, -2.336881798971000421E-14 ) ) ;
#2869=ORIENTED_EDGE ( 'NONE', *, *, #4706, .T. ) ;
#2938=DIRECTION ( 'NONE',  ( -2.580078660703000173E-14, 2.590196616235000036E-13, -1.000000000000000000 ) ) ;
#3008=CARTESIAN_POINT ( 'NONE',  ( 12.69999999999999929, -3576.320000000000164, 2270.760000000000218 ) ) ;
#3031=ORIENTED_EDGE ( 'NONE', *, *, #22869, .F. ) ;
#3141=CARTESIAN_POINT ( 'NONE',  ( 12.69999999999999929, -3574.034000000000106, 2239.391000000000076 ) ) ;
#3155=CYLINDRICAL_SURFACE ( 'NONE', #13555, 0.3810000000000011156 ) ;
#3204=ORIENTED_EDGE ( 'NONE', *, *, #21878, .T. ) ;
#3215=DIRECTION ( 'NONE',  ( 0.000000000000000000, 0.000000000000000000, 1.000000000000000000 ) ) ;
#3223=ORIENTED_EDGE ( 'NONE', *, *, #2554, .F. ) ;
#3234=CARTESIAN_POINT ( 'NONE',  ( 15.03168679717000167, -3580.841199999999844, 2242.820000000000164 ) ) ;
#3264=DIRECTION ( 'NONE',  ( 0.000000000000000000, -1.000000000000000000, 0.000000000000000000 ) ) ;
#3290=ORIENTED_EDGE ( 'NONE', *, *, #11778, .T. ) ;
#3312=AXIS2_PLACEMENT_3D ( 'NONE', #5858, #18707, #18486 ) ;
#3348=ADVANCED_FACE ( 'NONE', ( #23026 ), #12491, .T. ) ;
#3416=VERTEX_POINT ( 'NONE', #6655 ) ;
#3419=( NAMED_UNIT ( * ) PLANE_ANGLE_UNIT ( ) SI_UNIT ( $, .RADIAN. ) );
#3443=DIRECTION ( 'NONE',  ( 0.000000000000000000, 0.000000000000000000, -1.000000000000000000 ) ) ;
#3456=FACE_OUTER_BOUND ( 'NONE', #385, .T. ) ;
#3467=VECTOR ( 'NONE', #10156, 1000.000000000000000 ) ;
#3492=CARTESIAN_POINT ( 'NONE',  ( 10.36831320292846925, -3580.841200000038953, 2239.391000000000076 ) ) ;
#3528=DIRECTION ( 'NONE',  ( 0.8660254037825247941, 0.5000000000033149039, 0.000000000000000000 ) ) ;
#3549=ORIENTED_EDGE ( 'NONE', *, *, #17653, .F. ) ;
#3572=CARTESIAN_POINT ( 'NONE',  ( 18.16100000000000136, -3579.494999999999891, 2239.391000000000076 ) ) ;
#3607=VERTEX_POINT ( 'NONE', #9328 ) ;
#3652=FACE_OUTER_BOUND ( 'NONE', #13773, .T. ) ;
#3681=FACE_OUTER_BOUND ( 'NONE', #2689, .T. ) ;
#3688=DIRECTION ( 'NONE',  ( 0.000000000000000000, -1.000000000000000000, 0.000000000000000000 ) ) ;
#3760=CARTESIAN_POINT ( 'NONE',  ( 12.69999999999999929, -3579.494999999999891, 2239.391000000000076 ) ) ;
#3762=FACE_OUTER_BOUND ( 'NONE', #5461, .T. ) ;
#3801=DIRECTION ( 'NONE',  ( 0.000000000000000000, 0.000000000000000000, -1.000000000000000000 ) ) ;
#3818=CARTESIAN_POINT ( 'NONE',  ( 15.03168679716000078, -3578.148799999999937, 2242.820000000000164 ) ) ;
#3845=VERTEX_POINT ( 'NONE', #2588 ) ;
#3857=VERTEX_POINT ( 'NONE', #7633 ) ;
#3904=EDGE_CURVE ( 'NONE', #5428, #20995, #16739, .T. ) ;
#3926=CARTESIAN_POINT ( 'NONE',  ( 10.36831320286038327, -3578.148799999852145, 2239.167815367324692 ) ) ;
#3930=EDGE_CURVE ( 'NONE', #3416, #6172, #11956, .T. ) ;
#4058=ORIENTED_EDGE ( 'NONE', *, *, #15539, .T. ) ;
#4087=DIRECTION ( 'NONE',  ( 2.324635735433000053E-14, 0.000000000000000000, 1.000000000000000000 ) ) ;
#4113=PLANE ( 'NONE',  #19205 ) ;
#4142=ORIENTED_EDGE ( 'NONE', *, *, #13409, .T. ) ;
#4145=CARTESIAN_POINT ( 'NONE',  ( 12.70000000005999929, -3576.802599999999984, 2242.820000000000164 ) ) ;
#4169=DIRECTION ( 'NONE',  ( -2.848935406719999894E-12, 1.000000000000000000, 0.000000000000000000 ) ) ;
#4184=ORIENTED_EDGE ( 'NONE', *, *, #22869, .T. ) ;
#4212=DIRECTION ( 'NONE',  ( -0.8660254037816756956, 0.5000000000047857274, 0.000000000000000000 ) ) ;
#4226=AXIS2_PLACEMENT_3D ( 'NONE', #13025, #18829, #4772 ) ;
#4246=CIRCLE ( 'NONE', #19587, 1.269999999999882334 ) ;
#4280=ORIENTED_EDGE ( 'NONE', *, *, #18670, .T. ) ;
#4287=FACE_BOUND ( 'NONE', #18594, .T. ) ;
#4294=CIRCLE ( 'NONE', #9895, 3.175000000000149925 ) ;
#4374=DIRECTION ( 'NONE',  ( 0.8660254037822586737, -0.5000000000037757575, 0.000000000000000000 ) ) ;
#4390=ADVANCED_FACE ( 'NONE', ( #18718 ), #17195, .F. ) ;
#4451=CIRCLE ( 'NONE', #12691, 5.460999999999938126 ) ;
#4512=ORIENTED_EDGE ( 'NONE', *, *, #2138, .T. ) ;
#4550=DIRECTION ( 'NONE',  ( -2.324635735433000053E-14, 2.336881798971000105E-14, -1.000000000000000000 ) ) ;
#4598=VECTOR ( 'NONE', #4212, 999.9999999999998863 ) ;
#4619=LINE ( 'NONE', #11533, #18487 ) ;
#4661=CYLINDRICAL_SURFACE ( 'NONE', #20078, 0.3809999999998115450 ) ;
#4673=CARTESIAN_POINT ( 'NONE',  ( 10.36831320285999958, -3578.148799999999937, 2242.820000000000164 ) ) ;
#4701=CIRCLE ( 'NONE', #20428, 5.460999999999938126 ) ;
#4706=EDGE_CURVE ( 'NONE', #15456, #18476, #18472, .T. ) ;
#4737=ORIENTED_EDGE ( 'NONE', *, *, #12096, .F. ) ;
#4760=AXIS2_PLACEMENT_3D ( 'NONE', #1408, #16991, #13480 ) ;
#4772=DIRECTION ( 'NONE',  ( 0.000000000000000000, 0.000000000000000000, -1.000000000000000000 ) ) ;
#4791=VERTEX_POINT ( 'NONE', #9567 ) ;
#4817=DIRECTION ( 'NONE',  ( -2.626182175045999872E-12, 1.000000000000000000, 0.000000000000000000 ) ) ;
#4824=LINE ( 'NONE', #14093, #10208 ) ;
#4857=DIRECTION ( 'NONE',  ( -1.206643234470999950E-12, 1.000000000000000000, 0.000000000000000000 ) ) ;
#4907=ADVANCED_FACE ( 'NONE', ( #13426 ), #1848, .T. ) ;
#4911=CARTESIAN_POINT ( 'NONE',  ( 15.41268679716529455, -3581.061170452570423, 2239.009999999999764 ) ) ;
#4921=DIRECTION ( 'NONE',  ( -2.848935406719999894E-12, 1.000000000000000000, 2.336881798978000141E-14 ) ) ;
#4932=CARTESIAN_POINT ( 'NONE',  ( 12.69999999999999929, -3579.494999999999891, 2245.359999999999673 ) ) ;
#4966=DIRECTION ( 'NONE',  ( 0.000000000000000000, -1.000000000000000000, 0.000000000000000000 ) ) ;
#4977=CARTESIAN_POINT ( 'NONE',  ( 12.70000000003999929, -3582.187399999999798, 2242.820000000000164 ) ) ;
#5017=ORIENTED_EDGE ( 'NONE', *, *, #2428, .T. ) ;
#5035=ORIENTED_EDGE ( 'NONE', *, *, #10788, .T. ) ;
#5083=VECTOR ( 'NONE', #16492, 1000.000000000000000 ) ;
#5132=CARTESIAN_POINT ( 'NONE',  ( 12.69999999999999929, -3579.494999999999891, 2245.359999999999673 ) ) ;
#5161=ORIENTED_EDGE ( 'NONE', *, *, #10222, .F. ) ;
#5229=EDGE_CURVE ( 'NONE', #3857, #16025, #2177, .T. ) ;
#5287=DIRECTION ( 'NONE',  ( 0.000000000000000000, -2.336881798971000105E-14, 1.000000000000000000 ) ) ;
#5296=ORIENTED_EDGE ( 'NONE', *, *, #20664, .T. ) ;
#5334=AXIS2_PLACEMENT_3D ( 'NONE', #19630, #3801, #3688 ) ;
#5381=DIRECTION ( 'NONE',  ( 0.000000000000000000, 0.000000000000000000, 1.000000000000000000 ) ) ;
#5401=EDGE_CURVE ( 'NONE', #5562, #12834, #6361, .T. ) ;
#5417=VERTEX_POINT ( 'NONE', #21226 ) ;
#5422=DIRECTION ( 'NONE',  ( 1.000000000000000000, 5.432398939370943590E-28, -2.324635735433000369E-14 ) ) ;
#5423=DIRECTION ( 'NONE',  ( -2.324635735433000053E-14, 2.336881798971000105E-14, -1.000000000000000000 ) ) ;
#5428=VERTEX_POINT ( 'NONE', #7051 ) ;
#5457=AXIS2_PLACEMENT_3D ( 'NONE', #1123, #13329, #2550 ) ;
#5461=EDGE_LOOP ( 'NONE', ( #3204, #20639 ) ) ;
#5468=CARTESIAN_POINT ( 'NONE',  ( 10.36831320293797276, -3578.148799999986750, 2239.391000000000076 ) ) ;
#5479=DIRECTION ( 'NONE',  ( 0.000000000000000000, 0.000000000000000000, 1.000000000000000000 ) ) ;
#5497=AXIS2_PLACEMENT_3D ( 'NONE', #18975, #4550, #18849 ) ;
#5502=ORIENTED_EDGE ( 'NONE', *, *, #7294, .F. ) ;
#5562=VERTEX_POINT ( 'NONE', #11349 ) ;
#5597=DIRECTION ( 'NONE',  ( 5.432398939370942693E-28, 1.000000000000000000, 2.336881798971000105E-14 ) ) ;
#5599=FACE_OUTER_BOUND ( 'NONE', #12527, .T. ) ;
#5611=AXIS2_PLACEMENT_3D ( 'NONE', #2606, #9751, #7545 ) ;
#5641=( GEOMETRIC_REPRESENTATION_CONTEXT ( 3 ) GLOBAL_UNCERTAINTY_ASSIGNED_CONTEXT ( ( #22120 ) ) GLOBAL_UNIT_ASSIGNED_CONTEXT ( ( #7866, #11370, #22034 ) ) REPRESENTATION_CONTEXT ( 'NONE', 'WORKASPACE' ) );
#5648=LINE ( 'NONE', #19939, #1941 ) ;
#5709=CARTESIAN_POINT ( 'NONE',  ( 17.78000000000000114, -3579.494999999999891, 2239.391000000000076 ) ) ;
#5740=CARTESIAN_POINT ( 'NONE',  ( 17.78000000000000114, -3579.494999999999891, 2244.978999999999814 ) ) ;
#5790=CIRCLE ( 'NONE', #13259, 3.175000000000149925 ) ;
#5833=DIRECTION ( 'NONE',  ( -1.000000000000000000, -2.848935406719999894E-12, 0.000000000000000000 ) ) ;
#5836=PRODUCT_CONTEXT ( 'NONE', #9618, 'mechanical' ) ;
#5858=CARTESIAN_POINT ( 'NONE',  ( 12.69999999999999929, -3579.494999999999891, 2239.391000000000076 ) ) ;
#5938=ORIENTED_EDGE ( 'NONE', *, *, #55, .T. ) ;
#5970=AXIS2_PLACEMENT_3D ( 'NONE', #22322, #18693, #15422 ) ;
#5989=VECTOR ( 'NONE', #1217, 1000.000000000000000 ) ;
#6050=CARTESIAN_POINT ( 'NONE',  ( 12.69999999976711180, -3582.627340905157780, 2239.009999999999764 ) ) ;
#6066=DIRECTION ( 'NONE',  ( -0.8660254037821902839, 0.5000000000038942183, 1.814359422184980810E-12 ) ) ;
#6075=CARTESIAN_POINT ( 'NONE',  ( 9.987313202991520811, -3577.928829547366604, 2239.009999999999764 ) ) ;
#6104=EDGE_LOOP ( 'NONE', ( #19733, #8433, #271, #1335 ) ) ;
#6141=DIRECTION ( 'NONE',  ( 0.000000000000000000, 1.000000000000000000, 0.000000000000000000 ) ) ;
#6149=ORIENTED_EDGE ( 'NONE', *, *, #5401, .T. ) ;
#6172=VERTEX_POINT ( 'NONE', #8275 ) ;
#6198=ORIENTED_EDGE ( 'NONE', *, *, #11868, .F. ) ;
#6217=VECTOR ( 'NONE', #19417, 1000.000000000000114 ) ;
#6235=VERTEX_POINT ( 'NONE', #22325 ) ;
#6357=TOROIDAL_SURFACE ( 'NONE', #14964, 5.080000000000000071, 0.3810000000000000053 ) ;
#6361=( BOUNDED_CURVE ( )  B_SPLINE_CURVE ( 3, ( #18046, #7389, #14421, #9028 ),
 .UNSPECIFIED., .F., .T. ) 
 B_SPLINE_CURVE_WITH_KNOTS ( ( 4, 4 ),
 ( 1.570796326307487334, 3.141592653589783346 ),
 .UNSPECIFIED. ) 
 CURVE ( )  GEOMETRIC_REPRESENTATION_ITEM ( )  RATIONAL_B_SPLINE_CURVE ( ( 1.000000000000000000, 0.8047378540094838328, 0.8047378540094838328, 1.000000000000000000 ) ) 
 REPRESENTATION_ITEM ( '' )  );
#6369=CARTESIAN_POINT ( 'NONE',  ( 12.69999999999999929, -3579.494999999999891, 2270.760000000000218 ) ) ;
#6372=LINE ( 'NONE', #2506, #17088 ) ;
#6436=CARTESIAN_POINT ( 'NONE',  ( 12.69999999999999929, -3579.494999999999891, 2244.978999999999814 ) ) ;
#6535=FACE_OUTER_BOUND ( 'NONE', #14548, .T. ) ;
#6552=DIRECTION ( 'NONE',  ( 0.000000000000000000, -1.000000000000000000, 0.000000000000000000 ) ) ;
#6563=CARTESIAN_POINT ( 'NONE',  ( 7.238999999999998991, -3579.494999999999891, 2244.978999999999814 ) ) ;
#6614=AXIS2_PLACEMENT_3D ( 'NONE', #6369, #627, #6141 ) ;
#6621=ORIENTED_EDGE ( 'NONE', *, *, #12807, .T. ) ;
#6626=DIRECTION ( 'NONE',  ( -3.424927947642999691E-13, 2.590196616237999979E-13, -1.000000000000000000 ) ) ;
#6636=PLANE ( 'NONE',  #11344 ) ;
#6648=EDGE_CURVE ( 'NONE', #13538, #6235, #17448, .T. ) ;
#6655=CARTESIAN_POINT ( 'NONE',  ( 12.70000000005999929, -3576.802599999999984, 2242.820000000000164 ) ) ;
#6704=ORIENTED_EDGE ( 'NONE', *, *, #1364, .F. ) ;
#6851=VERTEX_POINT ( 'NONE', #22615 ) ;
#6905=CARTESIAN_POINT ( 'NONE',  ( 10.36831320285999958, -3580.841199999999844, 2242.820000000000164 ) ) ;
#6990=EDGE_LOOP ( 'NONE', ( #16800, #14570, #3223, #8322 ) ) ;
#7015=EDGE_CURVE ( 'NONE', #5417, #12899, #12190, .T. ) ;
#7051=CARTESIAN_POINT ( 'NONE',  ( 7.238999999999998991, -3579.494999999999891, 2239.391000000000531 ) ) ;
#7054=DIRECTION ( 'NONE',  ( -0.8660254037817188832, 0.5000000000047110094, 0.000000000000000000 ) ) ;
#7107=CARTESIAN_POINT ( 'NONE',  ( 10.21049783566652813, -3578.057685255121214, 2239.010000000076616 ) ) ;
#7142=EDGE_CURVE ( 'NONE', #3607, #15456, #12139, .T. ) ;
#7188=ORIENTED_EDGE ( 'NONE', *, *, #17653, .T. ) ;
#7220=EDGE_CURVE ( 'NONE', #12269, #4791, #16950, .T. ) ;
#7223=CARTESIAN_POINT ( 'NONE',  ( 15.18950216440284784, -3580.932314744898576, 2239.010000000038417 ) ) ;
#7231=VECTOR ( 'NONE', #15494, 1000.000000000000000 ) ;
#7234=CARTESIAN_POINT ( 'NONE',  ( 12.70000000002683471, -3576.620370510378052, 2239.010000000078435 ) ) ;
#7254=DIRECTION ( 'NONE',  ( 0.000000000000000000, -1.000000000000000000, 4.457650181899999573E-12 ) ) ;
#7294=EDGE_CURVE ( 'NONE', #6851, #13920, #8855, .T. ) ;
#7389=CARTESIAN_POINT ( 'NONE',  ( 15.18950216452952162, -3578.057685255022534, 2239.009999999890624 ) ) ;
#7448=ORIENTED_EDGE ( 'NONE', *, *, #12807, .F. ) ;
#7486=ORIENTED_EDGE ( 'NONE', *, *, #15017, .F. ) ;
#7512=EDGE_LOOP ( 'NONE', ( #13808, #16868, #4512, #5296 ) ) ;
#7545=DIRECTION ( 'NONE',  ( 1.000000000000000000, 0.000000000000000000, 0.000000000000000000 ) ) ;
#7633=CARTESIAN_POINT ( 'NONE',  ( 12.69999999999999929, -3584.956000000000131, 2244.978999999999814 ) ) ;
#7647=AXIS2_PLACEMENT_3D ( 'NONE', #5709, #5597, #5479 ) ;
#7725=ADVANCED_FACE ( 'NONE', ( #22485 ), #9013, .T. ) ;
#7804=DIRECTION ( 'NONE',  ( -0.5000000000047110094, -0.8660254037817188832, 0.000000000000000000 ) ) ;
#7866=( LENGTH_UNIT ( ) NAMED_UNIT ( * ) SI_UNIT ( .MILLI., .METRE. ) );
#7896=VECTOR ( 'NONE', #14949, 1000.000000000000000 ) ;
#7922=CARTESIAN_POINT ( 'NONE',  ( 12.69999999999999929, -3574.034000000000106, 2245.359999999999673 ) ) ;
#7968=DIRECTION ( 'NONE',  ( 1.206643234470999950E-12, -1.000000000000000000, -2.336881798973999985E-14 ) ) ;
#8056=PLANE ( 'NONE',  #5457 ) ;
#8063=ORIENTED_EDGE ( 'NONE', *, *, #20537, .T. ) ;
#8111=ADVANCED_FACE ( 'NONE', ( #13891 ), #17382, .T. ) ;
#8177=DIRECTION ( 'NONE',  ( 0.000000000000000000, -1.000000000000000000, 0.000000000000000000 ) ) ;
#8275=CARTESIAN_POINT ( 'NONE',  ( 12.70000000002640839, -3576.802599999929498, 2239.391000000000076 ) ) ;
#8303=EDGE_CURVE ( 'NONE', #6172, #23061, #6372, .T. ) ;
#8322=ORIENTED_EDGE ( 'NONE', *, *, #12974, .F. ) ;
#8352=CARTESIAN_POINT ( 'NONE',  ( 15.41268679715999923, -3577.928829547000078, 2239.009999999999764 ) ) ;
#8367=VERTEX_POINT ( 'NONE', #732 ) ;
#8383=DIRECTION ( 'NONE',  ( -0.8660254037817188832, 0.5000000000047110094, 3.181634500920069822E-14 ) ) ;
#8387=EDGE_CURVE ( 'NONE', #20995, #18145, #21964, .T. ) ;
#8433=ORIENTED_EDGE ( 'NONE', *, *, #21289, .F. ) ;
#8455=CARTESIAN_POINT ( 'NONE',  ( 12.70000000005999929, -3576.802599999999984, 2242.820000000000164 ) ) ;
#8508=CARTESIAN_POINT ( 'NONE',  ( 12.70000000005999929, -3576.362659094999799, 2239.009999999999764 ) ) ;
#8522=DIRECTION ( 'NONE',  ( -0.5000000000007065459, 0.8660254037840305896, 0.000000000000000000 ) ) ;
#8638=DIRECTION ( 'NONE',  ( -1.729311324296000017E-12, 1.000000000000000000, -3.793660610079000032E-12 ) ) ;
#8652=DIRECTION ( 'NONE',  ( -0.5000000000043351989, -0.8660254037819355988, 0.000000000000000000 ) ) ;
#8711=ADVANCED_FACE ( 'NONE', ( #14333, #3762 ), #1896, .T. ) ;
#8722=DIRECTION ( 'NONE',  ( -2.324635735433000053E-14, 0.000000000000000000, -1.000000000000000000 ) ) ;
#8841=TOROIDAL_SURFACE ( 'NONE', #18550, 5.080000000000000071, 0.3810000000000000053 ) ;
#8848=DIRECTION ( 'NONE',  ( -2.324635735433000053E-14, 2.336881798971000105E-14, -1.000000000000000000 ) ) ;
#8855=CIRCLE ( 'NONE', #17433, 3.175000000000149925 ) ;
#8912=VECTOR ( 'NONE', #20432, 1000.000000000000000 ) ;
#8961=CARTESIAN_POINT ( 'NONE',  ( 10.36831320285999958, -3580.841199999999844, 2239.391000000000076 ) ) ;
#9003=DIRECTION ( 'NONE',  ( 0.000000000000000000, 1.000000000000000000, 0.000000000000000000 ) ) ;
#9013=TOROIDAL_SURFACE ( 'NONE', #16858, 1.905000000000000027, 1.270000000000000018 ) ;
#9028=CARTESIAN_POINT ( 'NONE',  ( 15.03168679710029743, -3578.148799999889434, 2239.391000000000076 ) ) ;
#9052=ORIENTED_EDGE ( 'NONE', *, *, #19102, .T. ) ;
#9079=FACE_OUTER_BOUND ( 'NONE', #2296, .T. ) ;
#9140=ORIENTED_EDGE ( 'NONE', *, *, #10788, .F. ) ;
#9163=CARTESIAN_POINT ( 'NONE',  ( 10.36831320292846925, -3580.841200000038953, 2239.391000000000076 ) ) ;
#9196=AXIS2_PLACEMENT_3D ( 'NONE', #15807, #17792, #3264 ) ;
#9214=CARTESIAN_POINT ( 'NONE',  ( 12.69999999999999929, -3579.494999999999891, 2270.760000000000218 ) ) ;
#9231=CARTESIAN_POINT ( 'NONE',  ( 12.69999999999999929, -3579.494999999999891, 2270.760000000000218 ) ) ;
#9320=APPLICATION_CONTEXT ( 'configuration controlled 3d designs of mechanical parts and assemblies' ) ;
#9322=CARTESIAN_POINT ( 'NONE',  ( 12.69999999999999929, -3584.956000000000131, 2245.359999999999673 ) ) ;
#9328=CARTESIAN_POINT ( 'NONE',  ( 15.03168679717000167, -3580.841199999999844, 2242.820000000000164 ) ) ;
#9367=ADVANCED_FACE ( 'NONE', ( #2085 ), #21307, .T. ) ;
#9400=ORIENTED_EDGE ( 'NONE', *, *, #12293, .T. ) ;
#9477=PRODUCT_DEFINITION_CONTEXT ( 'detailed design', #9320, 'design' ) ;
#9522=CIRCLE ( 'NONE', #7647, 0.3809999999999647002 ) ;
#9535=VECTOR ( 'NONE', #6626, 1000.000000000000000 ) ;
#9543=DIRECTION ( 'NONE',  ( 0.8660254037817868289, -0.5000000000045929927, -1.484475890920977686E-12 ) ) ;
#9567=CARTESIAN_POINT ( 'NONE',  ( 15.03168679710930178, -3580.841200000109893, 2239.391000000000076 ) ) ;
#9618=APPLICATION_CONTEXT ( 'configuration controlled 3d designs of mechanical parts and assemblies' ) ;
#9669=DIRECTION ( 'NONE',  ( 0.8660254037841628172, 0.5000000000004778400, -5.443078266502769467E-12 ) ) ;
#9673=DIRECTION ( 'NONE',  ( -1.000000000000000000, 0.000000000000000000, 2.324635735433000053E-14 ) ) ;
#9751=DIRECTION ( 'NONE',  ( 0.000000000000000000, 0.000000000000000000, 1.000000000000000000 ) ) ;
#9765=ORIENTED_EDGE ( 'NONE', *, *, #22885, .T. ) ;
#9782=LINE ( 'NONE', #7922, #2660 ) ;
#9800=TOROIDAL_SURFACE ( 'NONE', #16551, 5.080000000000000071, 0.3810000000000000053 ) ;
#9828=CARTESIAN_POINT ( 'NONE',  ( 15.03168679717000167, -3580.841199999999844, 2239.391000000000076 ) ) ;
#9886=DIRECTION ( 'NONE',  ( 1.000000000000000000, 0.000000000000000000, 0.000000000000000000 ) ) ;
#9895=AXIS2_PLACEMENT_3D ( 'NONE', #11890, #3443, #15408 ) ;
#9899=ADVANCED_BREP_SHAPE_REPRESENTATION ( '', ( #13990, #5611 ), #5641 ) ;
#9919=ORIENTED_EDGE ( 'NONE', *, *, #19878, .F. ) ;
#9920=ORIENTED_EDGE ( 'NONE', *, *, #7015, .T. ) ;
#9975=ORIENTED_EDGE ( 'NONE', *, *, #19878, .T. ) ;
#10004=CARTESIAN_POINT ( 'NONE',  ( 12.69999999999999929, -3579.494999999999891, 2239.391000000000076 ) ) ;
#10016=CARTESIAN_POINT ( 'NONE',  ( 12.69999999999999929, -3579.494999999999891, 2272.030000000000200 ) ) ;
#10035=DIRECTION ( 'NONE',  ( 1.000000000000000000, 5.432398939370943590E-28, -2.324635735433000369E-14 ) ) ;
#10040=LINE ( 'NONE', #13563, #11670 ) ;
#10067=ORIENTED_EDGE ( 'NONE', *, *, #21289, .T. ) ;
#10108=PRODUCT ( 'Screw 7', 'Screw 7', '', ( #5836 ) ) ;
#10132=ORIENTED_EDGE ( 'NONE', *, *, #1364, .T. ) ;
#10145=EDGE_CURVE ( 'NONE', #17805, #16889, #16677, .T. ) ;
#10156=DIRECTION ( 'NONE',  ( 0.000000000000000000, 0.000000000000000000, -1.000000000000000000 ) ) ;
#10173=AXIS2_PLACEMENT_3D ( 'NONE', #17019, #2846, #1193 ) ;
#10174=FACE_OUTER_BOUND ( 'NONE', #1425, .T. ) ;
#10208=VECTOR ( 'NONE', #3528, 1000.000000000000000 ) ;
#10222=EDGE_CURVE ( 'NONE', #3845, #10958, #4701, .T. ) ;
#10235=CARTESIAN_POINT ( 'NONE',  ( 12.69999999999999929, -3579.494999999999891, 2239.391000000000076 ) ) ;
#10236=ORIENTED_EDGE ( 'NONE', *, *, #10145, .T. ) ;
#10245=FACE_OUTER_BOUND ( 'NONE', #16580, .T. ) ;
#10253=ADVANCED_FACE ( 'NONE', ( #13814 ), #4661, .T. ) ;
#10382=DIRECTION ( 'NONE',  ( -0.8660254037826616846, -0.5000000000030777603, 5.608020032299747518E-12 ) ) ;
#10386=ORIENTED_EDGE ( 'NONE', *, *, #14134, .F. ) ;
#10394=CYLINDRICAL_SURFACE ( 'NONE', #12071, 5.460999999999938126 ) ;
#10410=CARTESIAN_POINT ( 'NONE',  ( 9.987313202740898177, -3581.061170452786428, 2239.009999999999764 ) ) ;
#10485=LINE ( 'NONE', #8508, #11286 ) ;
#10598=ORIENTED_EDGE ( 'NONE', *, *, #5401, .F. ) ;
#10602=AXIS2_PLACEMENT_3D ( 'NONE', #4145, #13394, #18660 ) ;
#10656=ORIENTED_EDGE ( 'NONE', *, *, #20537, .F. ) ;
#10713=AXIS2_PLACEMENT_3D ( 'NONE', #10235, #8722, #4966 ) ;
#10774=EDGE_LOOP ( 'NONE', ( #22737, #17756, #19392, #13178 ) ) ;
#10784=EDGE_CURVE ( 'NONE', #2750, #22532, #16220, .T. ) ;
#10788=EDGE_CURVE ( 'NONE', #22778, #19756, #13337, .T. ) ;
#10838=ORIENTED_EDGE ( 'NONE', *, *, #14005, .T. ) ;
#10845=CARTESIAN_POINT ( 'NONE',  ( 15.03168679717383860, -3580.841200000147182, 2239.167815367294679 ) ) ;
#10859=ADVANCED_FACE ( 'NONE', ( #11355 ), #12220, .T. ) ;
#10861=EDGE_LOOP ( 'NONE', ( #5035, #19437, #14106, #15078 ) ) ;
#10872=( BOUNDED_CURVE ( )  B_SPLINE_CURVE ( 3, ( #5468, #3926, #7107, #14255 ),
 .UNSPECIFIED., .F., .T. ) 
 B_SPLINE_CURVE_WITH_KNOTS ( ( 4, 4 ),
 ( -2.664535259100375697E-14, 1.570796326449830138 ),
 .UNSPECIFIED. ) 
 CURVE ( )  GEOMETRIC_REPRESENTATION_ITEM ( )  RATIONAL_B_SPLINE_CURVE ( ( 1.000000000000000000, 0.8047378542056915496, 0.8047378542056915496, 1.000000000000000000 ) ) 
 REPRESENTATION_ITEM ( '' )  );
#10918=DIRECTION ( 'NONE',  ( -1.000000000000000000, 0.000000000000000000, 2.324635735433000053E-14 ) ) ;
#10933=PRODUCT_DEFINITION ( 'UNKNOWN', '', #13121, #9477 ) ;
#10958=VERTEX_POINT ( 'NONE', #6563 ) ;
#11024=EDGE_CURVE ( 'NONE', #2750, #19558, #18940, .T. ) ;
#11086=AXIS2_PLACEMENT_3D ( 'NONE', #19079, #1141, #19320 ) ;
#11119=DIRECTION ( 'NONE',  ( 0.000000000000000000, 0.000000000000000000, 1.000000000000000000 ) ) ;
#11151=DIRECTION ( 'NONE',  ( -0.5000000000031962211, 0.8660254037825932949, 0.000000000000000000 ) ) ;
#11164=ADVANCED_FACE ( 'NONE', ( #10174 ), #17319, .F. ) ;
#11173=EDGE_CURVE ( 'NONE', #12078, #23061, #2210, .T. ) ;
#11233=DIRECTION ( 'NONE',  ( 0.000000000000000000, -1.000000000000000000, 0.000000000000000000 ) ) ;
#11262=ORIENTED_EDGE ( 'NONE', *, *, #15017, .T. ) ;
#11286=VECTOR ( 'NONE', #21164, 1000.000000000000000 ) ;
#11316=ORIENTED_EDGE ( 'NONE', *, *, #12978, .F. ) ;
#11334=DIRECTION ( 'NONE',  ( 5.432398939370942693E-28, 1.000000000000000000, 2.336881798971000105E-14 ) ) ;
#11344=AXIS2_PLACEMENT_3D ( 'NONE', #13776, #20918, #4857 ) ;
#11346=VECTOR ( 'NONE', #4817, 1000.000000000000000 ) ;
#11349=CARTESIAN_POINT ( 'NONE',  ( 15.41268679728753099, -3577.928829547073747, 2239.009999999999764 ) ) ;
#11355=FACE_OUTER_BOUND ( 'NONE', #19470, .T. ) ;
#11370=( NAMED_UNIT ( * ) PLANE_ANGLE_UNIT ( ) SI_UNIT ( $, .RADIAN. ) );
#11385=ORIENTED_EDGE ( 'NONE', *, *, #2554, .T. ) ;
#11455=AXIS2_PLACEMENT_3D ( 'NONE', #2630, #20551, #9886 ) ;
#11479=ORIENTED_EDGE ( 'NONE', *, *, #2138, .F. ) ;
#11525=DIRECTION ( 'NONE',  ( 0.000000000000000000, 1.000000000000000000, 0.000000000000000000 ) ) ;
#11529=LINE ( 'NONE', #18677, #16280 ) ;
#11533=CARTESIAN_POINT ( 'NONE',  ( 10.36831320285999958, -3578.148799999999937, 2242.820000000000164 ) ) ;
#11558=ADVANCED_FACE ( 'NONE', ( #19997 ), #1946, .T. ) ;
#11583=LINE ( 'NONE', #9828, #12538 ) ;
#11613=DIRECTION ( 'NONE',  ( 0.8660254037820102058, -0.5000000000042060799, 0.000000000000000000 ) ) ;
#11618=DIRECTION ( 'NONE',  ( -1.000000000000000000, 1.224646799147353207E-16, 0.000000000000000000 ) ) ;
#11639=CARTESIAN_POINT ( 'NONE',  ( 12.70000000000865903, -3582.187400000168964, 2239.167815367317871 ) ) ;
#11670=VECTOR ( 'NONE', #8638, 1000.000000000000000 ) ;
#11672=DIRECTION ( 'NONE',  ( 0.8660254037825932949, 0.5000000000031962211, 0.000000000000000000 ) ) ;
#11692=ORIENTED_EDGE ( 'NONE', *, *, #16114, .F. ) ;
#11757=CARTESIAN_POINT ( 'NONE',  ( 9.987313202864001482, -3581.061170452999704, 2239.009999999999764 ) ) ;
#11778=EDGE_CURVE ( 'NONE', #16025, #5428, #16624, .T. ) ;
#11786=ORIENTED_EDGE ( 'NONE', *, *, #12978, .T. ) ;
#11798=CYLINDRICAL_SURFACE ( 'NONE', #20324, 0.3810000000000260956 ) ;
#11868=EDGE_CURVE ( 'NONE', #23061, #2750, #16758, .T. ) ;
#11890=CARTESIAN_POINT ( 'NONE',  ( 12.69999999999999929, -3579.494999999999891, 2245.359999999999673 ) ) ;
#11891=DIRECTION ( 'NONE',  ( -0.8660254037817187722, 0.5000000000047108983, 0.000000000000000000 ) ) ;
#11919=LINE ( 'NONE', #3008, #3467 ) ;
#11956=LINE ( 'NONE', #8455, #20132 ) ;
#12046=CARTESIAN_POINT ( 'NONE',  ( 11.34365660143000021, -3581.844255679000071, 2239.391000000000076 ) ) ;
#12053=DIRECTION ( 'NONE',  ( -2.903809793931999834E-13, 4.457650181899999573E-12, 1.000000000000000000 ) ) ;
#12071=AXIS2_PLACEMENT_3D ( 'NONE', #5132, #22450, #8177 ) ;
#12078=VERTEX_POINT ( 'NONE', #4673 ) ;
#12096=EDGE_CURVE ( 'NONE', #4791, #3607, #11583, .T. ) ;
#12128=EDGE_LOOP ( 'NONE', ( #13198, #9052, #14482, #10838 ) ) ;
#12139=LINE ( 'NONE', #3234, #12968 ) ;
#12170=CARTESIAN_POINT ( 'NONE',  ( 15.03168679716000078, -3578.148799999999937, 2242.820000000000164 ) ) ;
#12190=CIRCLE ( 'NONE', #15185, 5.080000000000000071 ) ;
#12220=TOROIDAL_SURFACE ( 'NONE', #5497, 5.080000000000000071, 0.3810000000000000053 ) ;
#12269=VERTEX_POINT ( 'NONE', #4911 ) ;
#12271=CARTESIAN_POINT ( 'NONE',  ( 12.70000000003999929, -3582.187399999999798, 2239.391000000000076 ) ) ;
#12293=EDGE_CURVE ( 'NONE', #5417, #8367, #17785, .T. ) ;
#12456=ADVANCED_FACE ( 'NONE', ( #20697 ), #8056, .T. ) ;
#12468=VERTEX_POINT ( 'NONE', #6075 ) ;
#12491=CYLINDRICAL_SURFACE ( 'NONE', #22686, 0.3809999999999154618 ) ;
#12492=DIRECTION ( 'NONE',  ( 0.000000000000000000, -1.000000000000000000, 0.000000000000000000 ) ) ;
#12527=EDGE_LOOP ( 'NONE', ( #16757, #15580, #1536, #21454 ) ) ;
#12538=VECTOR ( 'NONE', #1748, 1000.000000000000000 ) ;
#12556=ORIENTED_EDGE ( 'NONE', *, *, #21878, .F. ) ;
#12652=( BOUNDED_CURVE ( )  B_SPLINE_CURVE ( 3, ( #22419, #11639, #20665, #6050 ),
 .UNSPECIFIED., .F., .T. ) 
 B_SPLINE_CURVE_WITH_KNOTS ( ( 4, 4 ),
 ( 3.673835071120097305E-14, 1.570796326491086026 ),
 .UNSPECIFIED. ) 
 CURVE ( )  GEOMETRIC_REPRESENTATION_ITEM ( )  RATIONAL_B_SPLINE_CURVE ( ( 1.000000000000000000, 0.8047378541959824272, 0.8047378541959824272, 1.000000000000000000 ) ) 
 REPRESENTATION_ITEM ( '' )  );
#12691=AXIS2_PLACEMENT_3D ( 'NONE', #15411, #13888, #990 ) ;
#12714=CARTESIAN_POINT ( 'NONE',  ( 12.70000000028310616, -3576.362659094871105, 2239.009999999999764 ) ) ;
#12750=EDGE_LOOP ( 'NONE', ( #19356, #16022, #22316, #4737 ) ) ;
#12807=EDGE_CURVE ( 'NONE', #16889, #18145, #9522, .T. ) ;
#12834=VERTEX_POINT ( 'NONE', #16469 ) ;
#12860=AXIS2_PLACEMENT_3D ( 'NONE', #20152, #4087, #11233 ) ;
#12899=VERTEX_POINT ( 'NONE', #22308 ) ;
#12903=ORIENTED_EDGE ( 'NONE', *, *, #16114, .T. ) ;
#12968=VECTOR ( 'NONE', #10382, 1000.000000000000000 ) ;
#12969=FACE_OUTER_BOUND ( 'NONE', #7512, .T. ) ;
#12974=EDGE_CURVE ( 'NONE', #22532, #894, #12652, .T. ) ;
#12978=EDGE_CURVE ( 'NONE', #12078, #3416, #4619, .T. ) ;
#13014=ORIENTED_EDGE ( 'NONE', *, *, #13164, .T. ) ;
#13025=CARTESIAN_POINT ( 'NONE',  ( 12.69999999999999929, -3577.590000000000146, 2270.760000000000218 ) ) ;
#13030=SHAPE_REPRESENTATION_RELATIONSHIP ( 'NONE' , 'NONE' ,  #536, #9899 ) ;
#13075=DIRECTION ( 'NONE',  ( -2.324635735433000053E-14, 2.336881798971000105E-14, -1.000000000000000000 ) ) ;
#13121=PRODUCT_DEFINITION_FORMATION_WITH_SPECIFIED_SOURCE ( 'ANY', '', #10108, .NOT_KNOWN. ) ;
#13164=EDGE_CURVE ( 'NONE', #13920, #6851, #4294, .T. ) ;
#13178=ORIENTED_EDGE ( 'NONE', *, *, #19102, .F. ) ;
#13198=ORIENTED_EDGE ( 'NONE', *, *, #8303, .T. ) ;
#13199=CIRCLE ( 'NONE', #4226, 1.269999999999882334 ) ;
#13203=AXIS2_PLACEMENT_3D ( 'NONE', #13303, #5833, #4169 ) ;
#13259=AXIS2_PLACEMENT_3D ( 'NONE', #224, #5381, #9003 ) ;
#13284=DIRECTION ( 'NONE',  ( 0.000000000000000000, 0.000000000000000000, 1.000000000000000000 ) ) ;
#13303=CARTESIAN_POINT ( 'NONE',  ( 15.03168679717000167, -3580.841199999999844, 2242.820000000000164 ) ) ;
#13310=DIRECTION ( 'NONE',  ( 0.000000000000000000, 0.000000000000000000, -1.000000000000000000 ) ) ;
#13329=DIRECTION ( 'NONE',  ( 0.5000000000040877302, 0.8660254037820785955, 0.000000000000000000 ) ) ;
#13337=CIRCLE ( 'NONE', #6614, 3.175000000000149925 ) ;
#13390=LINE ( 'NONE', #20419, #21513 ) ;
#13392=ORIENTED_EDGE ( 'NONE', *, *, #22250, .F. ) ;
#13394=DIRECTION ( 'NONE',  ( 0.5000000000005969669, -0.8660254037840939834, 0.000000000000000000 ) ) ;
#13409=EDGE_CURVE ( 'NONE', #19558, #894, #13390, .T. ) ;
#13418=DIRECTION ( 'NONE',  ( 0.000000000000000000, -2.336881798971000105E-14, 1.000000000000000000 ) ) ;
#13426=FACE_OUTER_BOUND ( 'NONE', #10861, .T. ) ;
#13431=ORIENTED_EDGE ( 'NONE', *, *, #11024, .F. ) ;
#13480=DIRECTION ( 'NONE',  ( 0.000000000000000000, 0.000000000000000000, -1.000000000000000000 ) ) ;
#13538=VERTEX_POINT ( 'NONE', #13973 ) ;
#13544=EDGE_LOOP ( 'NONE', ( #16986, #9765 ) ) ;
#13555=AXIS2_PLACEMENT_3D ( 'NONE', #23068, #4921, #17331 ) ;
#13563=CARTESIAN_POINT ( 'NONE',  ( 15.03168679717000167, -3580.841199999999844, 2242.820000000000164 ) ) ;
#13613=CARTESIAN_POINT ( 'NONE',  ( 15.03168679717000167, -3580.841199999999844, 2239.391000000000076 ) ) ;
#13649=CARTESIAN_POINT ( 'NONE',  ( 12.69999999999999929, -3579.494999999999891, 2245.359999999999673 ) ) ;
#13703=DIRECTION ( 'NONE',  ( -1.000000000000000000, -1.165588477296754225E-12, 0.000000000000000000 ) ) ;
#13706=CIRCLE ( 'NONE', #11455, 5.080000000000000959 ) ;
#13718=DIRECTION ( 'NONE',  ( 0.000000000000000000, 1.000000000000000000, 0.000000000000000000 ) ) ;
#13735=LINE ( 'NONE', #19116, #14782 ) ;
#13773=EDGE_LOOP ( 'NONE', ( #16350, #3290, #1980, #12556, #7448 ) ) ;
#13776=CARTESIAN_POINT ( 'NONE',  ( 10.36831320285999958, -3578.148799999999937, 2242.820000000000164 ) ) ;
#13808=ORIENTED_EDGE ( 'NONE', *, *, #55, .F. ) ;
#13814=FACE_OUTER_BOUND ( 'NONE', #1602, .T. ) ;
#13815=CIRCLE ( 'NONE', #3312, 5.460999999999938126 ) ;
#13818=ADVANCED_FACE ( 'NONE', ( #17066 ), #11798, .T. ) ;
#13824=EDGE_CURVE ( 'NONE', #22778, #6851, #11919, .T. ) ;
#13837=EDGE_CURVE ( 'NONE', #22778, #13538, #13199, .T. ) ;
#13862=DIRECTION ( 'NONE',  ( 0.000000000000000000, 0.000000000000000000, -1.000000000000000000 ) ) ;
#13888=DIRECTION ( 'NONE',  ( 2.324635735433000053E-14, 0.000000000000000000, 1.000000000000000000 ) ) ;
#13891=FACE_OUTER_BOUND ( 'NONE', #15307, .T. ) ;
#13920=VERTEX_POINT ( 'NONE', #22798 ) ;
#13973=CARTESIAN_POINT ( 'NONE',  ( 12.69999999999999929, -3577.590000000000146, 2272.030000000000200 ) ) ;
#13986=CLOSED_SHELL ( 'NONE', ( #4907, #11558, #20122, #16856, #14732, #14967, #11164, #2412, #2656, #12456, #14296, #14448, #21825, #8111, #3348, #19672, #10253, #13818, #8711, #23104, #2093, #10859, #2347, #9367, #7725, #4390 ) ) ;
#13990=MANIFOLD_SOLID_BREP ( 'TORNILLO2[1]', #13986 ) ;
#13996=CARTESIAN_POINT ( 'NONE',  ( 15.03168679716000078, -3578.148799999999937, 2242.820000000000164 ) ) ;
#14005=EDGE_CURVE ( 'NONE', #15820, #6172, #22967, .T. ) ;
#14093=CARTESIAN_POINT ( 'NONE',  ( 12.70000000003999929, -3582.627340905000437, 2239.009999999999764 ) ) ;
#14106=ORIENTED_EDGE ( 'NONE', *, *, #6648, .F. ) ;
#14134=EDGE_CURVE ( 'NONE', #12899, #5417, #2359, .T. ) ;
#14146=CARTESIAN_POINT ( 'NONE',  ( 11.34365660145000021, -3577.145744321000166, 2239.391000000000076 ) ) ;
#14230=ORIENTED_EDGE ( 'NONE', *, *, #706, .F. ) ;
#14255=CARTESIAN_POINT ( 'NONE',  ( 9.987313202991520811, -3577.928829547366604, 2239.009999999999764 ) ) ;
#14296=ADVANCED_FACE ( 'NONE', ( #10245 ), #6636, .T. ) ;
#14333=FACE_BOUND ( 'NONE', #1098, .T. ) ;
#14411=ORIENTED_EDGE ( 'NONE', *, *, #13824, .F. ) ;
#14413=CIRCLE ( 'NONE', #10713, 5.460999999999938126 ) ;
#14421=CARTESIAN_POINT ( 'NONE',  ( 15.03168679716618605, -3578.148799999850326, 2239.167815367177809 ) ) ;
#14448=ADVANCED_FACE ( 'NONE', ( #9079 ), #173, .T. ) ;
#14482=ORIENTED_EDGE ( 'NONE', *, *, #15685, .F. ) ;
#14540=EDGE_CURVE ( 'NONE', #19756, #6235, #4246, .T. ) ;
#14548=EDGE_LOOP ( 'NONE', ( #10386, #12903, #4184, #9975, #17912 ) ) ;
#14560=CARTESIAN_POINT ( 'NONE',  ( 12.70000000003999929, -3582.187399999999798, 2242.820000000000164 ) ) ;
#14570=ORIENTED_EDGE ( 'NONE', *, *, #7220, .F. ) ;
#14684=EDGE_LOOP ( 'NONE', ( #5017, #18759, #5938, #10598 ) ) ;
#14721=ORIENTED_EDGE ( 'NONE', *, *, #10222, .T. ) ;
#14732=ADVANCED_FACE ( 'NONE', ( #3652 ), #9800, .T. ) ;
#14782=VECTOR ( 'NONE', #9543, 1000.000000000000114 ) ;
#14846=CARTESIAN_POINT ( 'NONE',  ( 12.69999999999999929, -3576.320000000000164, 2270.760000000000218 ) ) ;
#14949=DIRECTION ( 'NONE',  ( -1.082145837509000041E-12, 1.000000000000000000, 0.000000000000000000 ) ) ;
#14964=AXIS2_PLACEMENT_3D ( 'NONE', #21273, #8848, #1811 ) ;
#14967=ADVANCED_FACE ( 'NONE', ( #22833 ), #3155, .T. ) ;
#15009=ORIENTED_EDGE ( 'NONE', *, *, #8303, .F. ) ;
#15017=EDGE_CURVE ( 'NONE', #8367, #3845, #15433, .T. ) ;
#15044=DIRECTION ( 'NONE',  ( 1.000000000000000000, 0.000000000000000000, 0.000000000000000000 ) ) ;
#15078=ORIENTED_EDGE ( 'NONE', *, *, #13837, .F. ) ;
#15088=CARTESIAN_POINT ( 'NONE',  ( 12.69999999999999929, -3579.494999999999891, 2244.978999999999814 ) ) ;
#15147=ORIENTED_EDGE ( 'NONE', *, *, #5229, .F. ) ;
#15161=VECTOR ( 'NONE', #16410, 1000.000000000000000 ) ;
#15185=AXIS2_PLACEMENT_3D ( 'NONE', #4932, #5287, #23080 ) ;
#15307=EDGE_LOOP ( 'NONE', ( #3549, #6149, #18741, #2747 ) ) ;
#15323=CARTESIAN_POINT ( 'NONE',  ( 14.05634339859000015, -3581.844255679000071, 2239.391000000000076 ) ) ;
#15324=FACE_OUTER_BOUND ( 'NONE', #22345, .T. ) ;
#15371=LINE ( 'NONE', #13613, #11346 ) ;
#15408=DIRECTION ( 'NONE',  ( 5.572969907074833723E-14, -1.000000000000000000, 0.000000000000000000 ) ) ;
#15411=CARTESIAN_POINT ( 'NONE',  ( 12.69999999999999929, -3579.494999999999891, 2244.978999999999814 ) ) ;
#15422=DIRECTION ( 'NONE',  ( 0.000000000000000000, 1.000000000000000000, 0.000000000000000000 ) ) ;
#15433=CIRCLE ( 'NONE', #12860, 5.460999999999938126 ) ;
#15456=VERTEX_POINT ( 'NONE', #21419 ) ;
#15458=FACE_OUTER_BOUND ( 'NONE', #10774, .T. ) ;
#15494=DIRECTION ( 'NONE',  ( 1.690229834190999937E-12, -1.000000000000000000, 0.000000000000000000 ) ) ;
#15539=EDGE_CURVE ( 'NONE', #3845, #17805, #9782, .T. ) ;
#15554=CARTESIAN_POINT ( 'NONE',  ( 12.70000000002484875, -3582.187400000083926, 2239.391000000000076 ) ) ;
#15567=ORIENTED_EDGE ( 'NONE', *, *, #18670, .F. ) ;
#15569=DIRECTION ( 'NONE',  ( 0.000000000000000000, 0.000000000000000000, -1.000000000000000000 ) ) ;
#15580=ORIENTED_EDGE ( 'NONE', *, *, #20664, .F. ) ;
#15635=AXIS2_PLACEMENT_3D ( 'NONE', #9231, #16372, #323 ) ;
#15684=DIRECTION ( 'NONE',  ( 2.324635735433000053E-14, 0.000000000000000000, 1.000000000000000000 ) ) ;
#15685=EDGE_CURVE ( 'NONE', #15820, #12468, #10485, .T. ) ;
#15764=DIRECTION ( 'NONE',  ( 0.5000000000048030468, 0.8660254037816655925, 0.000000000000000000 ) ) ;
#15807=CARTESIAN_POINT ( 'NONE',  ( 12.69999999999999929, -3579.494999999999891, 2244.978999999999814 ) ) ;
#15820=VERTEX_POINT ( 'NONE', #12714 ) ;
#15910=DIRECTION ( 'NONE',  ( 0.000000000000000000, 0.000000000000000000, 1.000000000000000000 ) ) ;
#15980=ORIENTED_EDGE ( 'NONE', *, *, #5229, .T. ) ;
#16022=ORIENTED_EDGE ( 'NONE', *, *, #23003, .F. ) ;
#16025=VERTEX_POINT ( 'NONE', #21016 ) ;
#16040=CARTESIAN_POINT ( 'NONE',  ( 10.36831320286361979, -3580.841200000155368, 2239.167815367206913 ) ) ;
#16114=EDGE_CURVE ( 'NONE', #12899, #10958, #20290, .T. ) ;
#16194=DIRECTION ( 'NONE',  ( 0.000000000000000000, 0.000000000000000000, 1.000000000000000000 ) ) ;
#16220=LINE ( 'NONE', #8961, #1749 ) ;
#16280=VECTOR ( 'NONE', #2623, 1000.000000000000000 ) ;
#16296=CARTESIAN_POINT ( 'NONE',  ( 10.36831320285999958, -3578.148799999999937, 2239.391000000000076 ) ) ;
#16298=CIRCLE ( 'NONE', #9196, 5.460999999999938126 ) ;
#16350=ORIENTED_EDGE ( 'NONE', *, *, #22250, .T. ) ;
#16355=DIRECTION ( 'NONE',  ( 0.000000000000000000, 0.000000000000000000, -1.000000000000000000 ) ) ;
#16372=DIRECTION ( 'NONE',  ( 0.000000000000000000, 0.000000000000000000, -1.000000000000000000 ) ) ;
#16410=DIRECTION ( 'NONE',  ( 1.278298683861999854E-12, -1.000000000000000000, 0.000000000000000000 ) ) ;
#16469=CARTESIAN_POINT ( 'NONE',  ( 15.03168679710029743, -3578.148799999889434, 2239.391000000000076 ) ) ;
#16492=DIRECTION ( 'NONE',  ( -2.170301461641000033E-13, -2.590196616223999907E-13, -1.000000000000000000 ) ) ;
#16529=FACE_OUTER_BOUND ( 'NONE', #12750, .T. ) ;
#16551=AXIS2_PLACEMENT_3D ( 'NONE', #3760, #1894, #5422 ) ;
#16580=EDGE_LOOP ( 'NONE', ( #6198, #22947, #10132, #10067 ) ) ;
#16590=CARTESIAN_POINT ( 'NONE',  ( 12.70000000028310616, -3576.362659094871105, 2239.009999999999764 ) ) ;
#16612=CARTESIAN_POINT ( 'NONE',  ( 10.36831320285999958, -3580.841199999999844, 2242.820000000000164 ) ) ;
#16624=CIRCLE ( 'NONE', #20745, 5.460999999999938126 ) ;
#16677=CIRCLE ( 'NONE', #11086, 5.460999999999938126 ) ;
#16739=CIRCLE ( 'NONE', #4760, 0.3809999999999647002 ) ;
#16741=UNCERTAINTY_MEASURE_WITH_UNIT (LENGTH_MEASURE( 1.000000000000000082E-05 ), #21126, 'distance_accuracy_value', 'NONE');
#16756=CARTESIAN_POINT ( 'NONE',  ( 9.987313202740898177, -3581.061170452786428, 2239.009999999999764 ) ) ;
#16757=ORIENTED_EDGE ( 'NONE', *, *, #18178, .F. ) ;
#16758=LINE ( 'NONE', #16296, #15161 ) ;
#16800=ORIENTED_EDGE ( 'NONE', *, *, #21535, .T. ) ;
#16856=ADVANCED_FACE ( 'NONE', ( #3456 ), #21735, .T. ) ;
#16858=AXIS2_PLACEMENT_3D ( 'NONE', #19653, #15910, #13718 ) ;
#16868=ORIENTED_EDGE ( 'NONE', *, *, #12096, .T. ) ;
#16889=VERTEX_POINT ( 'NONE', #3572 ) ;
#16950=( BOUNDED_CURVE ( )  B_SPLINE_CURVE ( 3, ( #21291, #7223, #10845, #21402 ),
 .UNSPECIFIED., .F., .T. ) 
 B_SPLINE_CURVE_WITH_KNOTS ( ( 4, 4 ),
 ( 1.570796326968375789, 3.141592653589766471 ),
 .UNSPECIFIED. ) 
 CURVE ( )  GEOMETRIC_REPRESENTATION_ITEM ( )  RATIONAL_B_SPLINE_CURVE ( ( 1.000000000000000000, 0.8047378541652607797, 0.8047378541652607797, 1.000000000000000000 ) ) 
 REPRESENTATION_ITEM ( '' )  );
#16959=ORIENTED_EDGE ( 'NONE', *, *, #11778, .F. ) ;
#16986=ORIENTED_EDGE ( 'NONE', *, *, #6648, .T. ) ;
#16991=DIRECTION ( 'NONE',  ( 1.224646799141920914E-16, -1.000000000000000000, -2.336881798971000421E-14 ) ) ;
#17004=CARTESIAN_POINT ( 'NONE',  ( 7.619999999999999218, -3579.494999999999891, 2239.009999999999764 ) ) ;
#17019=CARTESIAN_POINT ( 'NONE',  ( 7.619999999999999218, -3579.494999999999891, 2244.978999999999814 ) ) ;
#17066=FACE_OUTER_BOUND ( 'NONE', #6990, .T. ) ;
#17088=VECTOR ( 'NONE', #22174, 1000.000000000000000 ) ;
#17157=CARTESIAN_POINT ( 'NONE',  ( 12.70000000002640661, -3576.802599999840822, 2239.167815367326057 ) ) ;
#17195=PLANE ( 'NONE',  #2251 ) ;
#17212=PRODUCT_DEFINITION_SHAPE ( 'NONE', 'NONE',  #10933 ) ;
#17231=ORIENTED_EDGE ( 'NONE', *, *, #15685, .T. ) ;
#17271=LINE ( 'NONE', #4977, #5989 ) ;
#17319=PLANE ( 'NONE',  #2472 ) ;
#17331=DIRECTION ( 'NONE',  ( 1.000000000000000000, 2.331176954593497545E-12, 0.000000000000000000 ) ) ;
#17382=CYLINDRICAL_SURFACE ( 'NONE', #22297, 0.3809999999999303388 ) ;
#17433=AXIS2_PLACEMENT_3D ( 'NONE', #22864, #13862, #1311 ) ;
#17448=CIRCLE ( 'NONE', #18575, 1.904999999999823501 ) ;
#17577=ORIENTED_EDGE ( 'NONE', *, *, #13409, .F. ) ;
#17653=EDGE_CURVE ( 'NONE', #5562, #15820, #21909, .T. ) ;
#17756=ORIENTED_EDGE ( 'NONE', *, *, #11024, .T. ) ;
#17785=CIRCLE ( 'NONE', #2074, 0.3809999999999647002 ) ;
#17792=DIRECTION ( 'NONE',  ( 2.324635735433000053E-14, 0.000000000000000000, 1.000000000000000000 ) ) ;
#17805=VERTEX_POINT ( 'NONE', #3141 ) ;
#17815=LINE ( 'NONE', #1768, #20704 ) ;
#17912=ORIENTED_EDGE ( 'NONE', *, *, #12293, .F. ) ;
#17975=ORIENTED_EDGE ( 'NONE', *, *, #12974, .T. ) ;
#17982=VERTEX_POINT ( 'NONE', #12170 ) ;
#18046=CARTESIAN_POINT ( 'NONE',  ( 15.41268679728753099, -3577.928829547073747, 2239.009999999999764 ) ) ;
#18061=AXIS2_PLACEMENT_3D ( 'NONE', #13649, #13418, #22311 ) ;
#18145=VERTEX_POINT ( 'NONE', #12 ) ;
#18173=DIRECTION ( 'NONE',  ( 7.280632624815999719E-13, -1.000000000000000000, 4.288485907148999414E-12 ) ) ;
#18178=EDGE_CURVE ( 'NONE', #12834, #6172, #17815, .T. ) ;
#18472=LINE ( 'NONE', #20133, #21717 ) ;
#18476=VERTEX_POINT ( 'NONE', #6905 ) ;
#18486=DIRECTION ( 'NONE',  ( 0.000000000000000000, -1.000000000000000000, 0.000000000000000000 ) ) ;
#18487=VECTOR ( 'NONE', #9669, 999.9999999999998863 ) ;
#18550=AXIS2_PLACEMENT_3D ( 'NONE', #15088, #18824, #10035 ) ;
#18575=AXIS2_PLACEMENT_3D ( 'NONE', #22645, #13284, #11525 ) ;
#18594=EDGE_LOOP ( 'NONE', ( #13014, #19030 ) ) ;
#18660=DIRECTION ( 'NONE',  ( 0.000000000000000000, 0.000000000000000000, -1.000000000000000000 ) ) ;
#18670=EDGE_CURVE ( 'NONE', #19756, #22778, #5790, .T. ) ;
#18677=CARTESIAN_POINT ( 'NONE',  ( 12.69999999999999929, -3582.670000000000073, 2270.760000000000218 ) ) ;
#18680=LINE ( 'NONE', #11757, #7896 ) ;
#18693=DIRECTION ( 'NONE',  ( 0.000000000000000000, 0.000000000000000000, 1.000000000000000000 ) ) ;
#18707=DIRECTION ( 'NONE',  ( -2.324635735433000053E-14, 0.000000000000000000, -1.000000000000000000 ) ) ;
#18718=FACE_OUTER_BOUND ( 'NONE', #13544, .T. ) ;
#18741=ORIENTED_EDGE ( 'NONE', *, *, #18178, .T. ) ;
#18759=ORIENTED_EDGE ( 'NONE', *, *, #7220, .T. ) ;
#18773=CARTESIAN_POINT ( 'NONE',  ( 12.69999999999999929, -3579.494999999999891, 2239.009999999999764 ) ) ;
#18824=DIRECTION ( 'NONE',  ( -2.324635735433000053E-14, 2.336881798971000105E-14, -1.000000000000000000 ) ) ;
#18829=DIRECTION ( 'NONE',  ( 1.000000000000000000, 0.000000000000000000, 0.000000000000000000 ) ) ;
#18849=DIRECTION ( 'NONE',  ( 1.000000000000000000, 5.432398939370943590E-28, -2.324635735433000369E-14 ) ) ;
#18940=( BOUNDED_CURVE ( )  B_SPLINE_CURVE ( 3, ( #3492, #16040, #23057, #10410 ),
 .UNSPECIFIED., .F., .T. ) 
 B_SPLINE_CURVE_WITH_KNOTS ( ( 4, 4 ),
 ( -9.769962616701377556E-15, 1.570796327117804925 ),
 .UNSPECIFIED. ) 
 CURVE ( )  GEOMETRIC_REPRESENTATION_ITEM ( )  RATIONAL_B_SPLINE_CURVE ( ( 1.000000000000000000, 0.8047378540482524878, 0.8047378540482524878, 1.000000000000000000 ) ) 
 REPRESENTATION_ITEM ( '' )  );
#18975=CARTESIAN_POINT ( 'NONE',  ( 12.69999999999999929, -3579.494999999999891, 2244.978999999999814 ) ) ;
#19030=ORIENTED_EDGE ( 'NONE', *, *, #7294, .T. ) ;
#19066=DIRECTION ( 'NONE',  ( 0.5000000000031612490, -0.8660254037826135010, 0.000000000000000000 ) ) ;
#19079=CARTESIAN_POINT ( 'NONE',  ( 12.69999999999999929, -3579.494999999999891, 2239.391000000000076 ) ) ;
#19102=EDGE_CURVE ( 'NONE', #23061, #12468, #10872, .T. ) ;
#19116=CARTESIAN_POINT ( 'NONE',  ( 12.70000000005999929, -3576.802599999999984, 2242.820000000000164 ) ) ;
#19205=AXIS2_PLACEMENT_3D ( 'NONE', #14560, #11151, #16194 ) ;
#19257=EDGE_CURVE ( 'NONE', #3416, #17982, #13735, .T. ) ;
#19312=VECTOR ( 'NONE', #21464, 1000.000000000000000 ) ;
#19320=DIRECTION ( 'NONE',  ( 0.000000000000000000, -1.000000000000000000, 0.000000000000000000 ) ) ;
#19356=ORIENTED_EDGE ( 'NONE', *, *, #21535, .F. ) ;
#19362=AXIS2_PLACEMENT_3D ( 'NONE', #21594, #5423, #10918 ) ;
#19392=ORIENTED_EDGE ( 'NONE', *, *, #706, .T. ) ;
#19417=DIRECTION ( 'NONE',  ( 0.8660254037827048723, 0.5000000000030029312, 0.000000000000000000 ) ) ;
#19437=ORIENTED_EDGE ( 'NONE', *, *, #14540, .T. ) ;
#19470=EDGE_LOOP ( 'NONE', ( #11692, #20241, #9400, #11262, #14721 ) ) ;
#19558=VERTEX_POINT ( 'NONE', #16756 ) ;
#19587=AXIS2_PLACEMENT_3D ( 'NONE', #2837, #11618, #2718 ) ;
#19630=CARTESIAN_POINT ( 'NONE',  ( 12.69999999999999929, -3579.494999999999891, 2245.359999999999673 ) ) ;
#19653=CARTESIAN_POINT ( 'NONE',  ( 12.69999999999999929, -3579.494999999999891, 2270.760000000000218 ) ) ;
#19672=ADVANCED_FACE ( 'NONE', ( #15458 ), #1035, .T. ) ;
#19725=ORIENTED_EDGE ( 'NONE', *, *, #11173, .T. ) ;
#19733=ORIENTED_EDGE ( 'NONE', *, *, #10784, .F. ) ;
#19756=VERTEX_POINT ( 'NONE', #20605 ) ;
#19833=ORIENTED_EDGE ( 'NONE', *, *, #3930, .F. ) ;
#19852=CARTESIAN_POINT ( 'NONE',  ( 12.69999999976711180, -3582.627340905157780, 2239.009999999999764 ) ) ;
#19864=ORIENTED_EDGE ( 'NONE', *, *, #20568, .F. ) ;
#19878=EDGE_CURVE ( 'NONE', #3857, #8367, #16298, .T. ) ;
#19880=EDGE_LOOP ( 'NONE', ( #14411, #15567, #8063, #5502 ) ) ;
#19883=PLANE ( 'NONE',  #960 ) ;
#19905=CARTESIAN_POINT ( 'NONE',  ( 10.36831320285999958, -3578.148799999999937, 2242.820000000000164 ) ) ;
#19939=CARTESIAN_POINT ( 'NONE',  ( 10.36831320285999958, -3578.148799999999937, 2242.820000000000164 ) ) ;
#19997=FACE_OUTER_BOUND ( 'NONE', #1843, .T. ) ;
#20025=AXIS2_PLACEMENT_3D ( 'NONE', #9214, #16355, #12492 ) ;
#20078=AXIS2_PLACEMENT_3D ( 'NONE', #12046, #22926, #8652 ) ;
#20122=ADVANCED_FACE ( 'NONE', ( #6535 ), #8841, .T. ) ;
#20132=VECTOR ( 'NONE', #2938, 1000.000000000000000 ) ;
#20133=CARTESIAN_POINT ( 'NONE',  ( 12.70000000003999929, -3582.187399999999798, 2242.820000000000164 ) ) ;
#20152=CARTESIAN_POINT ( 'NONE',  ( 12.69999999999999929, -3579.494999999999891, 2244.978999999999814 ) ) ;
#20227=PLANE ( 'NONE',  #13203 ) ;
#20241=ORIENTED_EDGE ( 'NONE', *, *, #7015, .F. ) ;
#20290=CIRCLE ( 'NONE', #10173, 0.3809999999999647002 ) ;
#20324=AXIS2_PLACEMENT_3D ( 'NONE', #15323, #11672, #19066 ) ;
#20325=AXIS2_PLACEMENT_3D ( 'NONE', #21869, #13075, #9673 ) ;
#20419=CARTESIAN_POINT ( 'NONE',  ( 9.987313202864001482, -3581.061170452999704, 2239.009999999999764 ) ) ;
#20428=AXIS2_PLACEMENT_3D ( 'NONE', #6436, #15684, #20956 ) ;
#20432=DIRECTION ( 'NONE',  ( 0.000000000000000000, 0.000000000000000000, -1.000000000000000000 ) ) ;
#20462=AXIS2_PLACEMENT_3D ( 'NONE', #18773, #2719, #15044 ) ;
#20502=EDGE_LOOP ( 'NONE', ( #21834, #4280, #20560, #22019 ) ) ;
#20535=AXIS2_PLACEMENT_3D ( 'NONE', #10016, #3215, #20553 ) ;
#20537=EDGE_CURVE ( 'NONE', #19756, #13920, #11529, .T. ) ;
#20551=DIRECTION ( 'NONE',  ( 0.000000000000000000, 2.336881798971000105E-14, -1.000000000000000000 ) ) ;
#20553=DIRECTION ( 'NONE',  ( 0.000000000000000000, 1.000000000000000000, 0.000000000000000000 ) ) ;
#20560=ORIENTED_EDGE ( 'NONE', *, *, #13837, .T. ) ;
#20568=EDGE_CURVE ( 'NONE', #5428, #17805, #14413, .T. ) ;
#20605=CARTESIAN_POINT ( 'NONE',  ( 12.69999999999999929, -3582.670000000000073, 2270.760000000000218 ) ) ;
#20639=ORIENTED_EDGE ( 'NONE', *, *, #8387, .T. ) ;
#20664=EDGE_CURVE ( 'NONE', #17982, #12834, #21027, .T. ) ;
#20665=CARTESIAN_POINT ( 'NONE',  ( 12.70000000000855955, -3582.369629489642193, 2239.010000000067976 ) ) ;
#20697=FACE_OUTER_BOUND ( 'NONE', #6104, .T. ) ;
#20704=VECTOR ( 'NONE', #7054, 999.9999999999998863 ) ;
#20745=AXIS2_PLACEMENT_3D ( 'NONE', #10004, #21346, #23083 ) ;
#20840=CARTESIAN_POINT ( 'NONE',  ( 12.69999999999999929, -3579.494999999999891, 2272.030000000000200 ) ) ;
#20918=DIRECTION ( 'NONE',  ( 1.000000000000000000, 1.206643234470999950E-12, 0.000000000000000000 ) ) ;
#20956=DIRECTION ( 'NONE',  ( 0.000000000000000000, -1.000000000000000000, 0.000000000000000000 ) ) ;
#20995=VERTEX_POINT ( 'NONE', #17004 ) ;
#21016=CARTESIAN_POINT ( 'NONE',  ( 12.69999999999999929, -3584.956000000000131, 2239.391000000000076 ) ) ;
#21027=LINE ( 'NONE', #13996, #9535 ) ;
#21029=ORIENTED_EDGE ( 'NONE', *, *, #15539, .F. ) ;
#21126=( LENGTH_UNIT ( ) NAMED_UNIT ( * ) SI_UNIT ( .MILLI., .METRE. ) );
#21164=DIRECTION ( 'NONE',  ( -0.8660254037839826280, -0.5000000000007898127, 0.000000000000000000 ) ) ;
#21167=ORIENTED_EDGE ( 'NONE', *, *, #19257, .T. ) ;
#21226=CARTESIAN_POINT ( 'NONE',  ( 17.78000000000000114, -3579.494999999999891, 2245.359999999999673 ) ) ;
#21273=CARTESIAN_POINT ( 'NONE',  ( 12.69999999999999929, -3579.494999999999891, 2239.391000000000076 ) ) ;
#21289=EDGE_CURVE ( 'NONE', #18476, #2750, #450, .T. ) ;
#21291=CARTESIAN_POINT ( 'NONE',  ( 15.41268679716529455, -3581.061170452570423, 2239.009999999999764 ) ) ;
#21307=CYLINDRICAL_SURFACE ( 'NONE', #15635, 3.175000000000149925 ) ;
#21346=DIRECTION ( 'NONE',  ( -2.324635735433000053E-14, 0.000000000000000000, -1.000000000000000000 ) ) ;
#21402=CARTESIAN_POINT ( 'NONE',  ( 15.03168679710930178, -3580.841200000109893, 2239.391000000000076 ) ) ;
#21419=CARTESIAN_POINT ( 'NONE',  ( 12.70000000003999929, -3582.187399999999798, 2242.820000000000164 ) ) ;
#21454=ORIENTED_EDGE ( 'NONE', *, *, #3930, .T. ) ;
#21464=DIRECTION ( 'NONE',  ( 2.150065550568999996E-13, 0.000000000000000000, -1.000000000000000000 ) ) ;
#21513=VECTOR ( 'NONE', #11613, 1000.000000000000114 ) ;
#21535=EDGE_CURVE ( 'NONE', #22532, #4791, #1476, .T. ) ;
#21594=CARTESIAN_POINT ( 'NONE',  ( 12.69999999999999929, -3579.494999999999891, 2239.009999999999764 ) ) ;
#21717=VECTOR ( 'NONE', #6066, 1000.000000000000000 ) ;
#21721=ORIENTED_EDGE ( 'NONE', *, *, #3904, .F. ) ;
#21735=CYLINDRICAL_SURFACE ( 'NONE', #5334, 5.460999999999938126 ) ;
#21825=ADVANCED_FACE ( 'NONE', ( #5599 ), #19883, .T. ) ;
#21834=ORIENTED_EDGE ( 'NONE', *, *, #14540, .F. ) ;
#21869=CARTESIAN_POINT ( 'NONE',  ( 12.69999999999999929, -3579.494999999999891, 2245.359999999999673 ) ) ;
#21872=SHAPE_DEFINITION_REPRESENTATION ( #17212, #536 ) ;
#21878=EDGE_CURVE ( 'NONE', #18145, #20995, #13706, .T. ) ;
#21909=LINE ( 'NONE', #2342, #4598 ) ;
#21964=CIRCLE ( 'NONE', #20462, 5.080000000000000959 ) ;
#22019=ORIENTED_EDGE ( 'NONE', *, *, #22885, .F. ) ;
#22034=( NAMED_UNIT ( * ) SI_UNIT ( $, .STERADIAN. ) SOLID_ANGLE_UNIT ( ) );
#22085=PLANE ( 'NONE',  #20325 ) ;
#22120=UNCERTAINTY_MEASURE_WITH_UNIT (LENGTH_MEASURE( 1.000000000000000082E-05 ), #7866, 'distance_accuracy_value', 'NONE');
#22174=DIRECTION ( 'NONE',  ( -0.8660254037840939834, -0.5000000000005969669, 0.000000000000000000 ) ) ;
#22191=ORIENTED_EDGE ( 'NONE', *, *, #10784, .T. ) ;
#22216=ORIENTED_EDGE ( 'NONE', *, *, #8387, .F. ) ;
#22250=EDGE_CURVE ( 'NONE', #16889, #16025, #13815, .T. ) ;
#22297=AXIS2_PLACEMENT_3D ( 'NONE', #22664, #8383, #15764 ) ;
#22308=CARTESIAN_POINT ( 'NONE',  ( 7.619999999999999218, -3579.494999999999891, 2245.359999999999673 ) ) ;
#22311=DIRECTION ( 'NONE',  ( -1.000000000000000000, 0.000000000000000000, 0.000000000000000000 ) ) ;
#22316=ORIENTED_EDGE ( 'NONE', *, *, #7142, .F. ) ;
#22322=CARTESIAN_POINT ( 'NONE',  ( 12.69999999999999929, -3579.494999999999891, 2270.760000000000218 ) ) ;
#22325=CARTESIAN_POINT ( 'NONE',  ( 12.69999999999999929, -3581.400000000000091, 2272.030000000000200 ) ) ;
#22345=EDGE_LOOP ( 'NONE', ( #21029, #7486, #9919, #15980, #13392, #748 ) ) ;
#22360=CARTESIAN_POINT ( 'NONE',  ( 9.987313202862001305, -3579.494999999999891, 2239.391000000000076 ) ) ;
#22419=CARTESIAN_POINT ( 'NONE',  ( 12.70000000002484875, -3582.187400000083926, 2239.391000000000076 ) ) ;
#22450=DIRECTION ( 'NONE',  ( 0.000000000000000000, 0.000000000000000000, -1.000000000000000000 ) ) ;
#22485=FACE_OUTER_BOUND ( 'NONE', #20502, .T. ) ;
#22532=VERTEX_POINT ( 'NONE', #15554 ) ;
#22615=CARTESIAN_POINT ( 'NONE',  ( 12.69999999999999929, -3576.320000000000164, 2245.359999999999673 ) ) ;
#22645=CARTESIAN_POINT ( 'NONE',  ( 12.69999999999999929, -3579.494999999999891, 2272.030000000000200 ) ) ;
#22664=CARTESIAN_POINT ( 'NONE',  ( 14.05634339859000015, -3577.145744321000166, 2239.391000000000076 ) ) ;
#22686=AXIS2_PLACEMENT_3D ( 'NONE', #14146, #1240, #8522 ) ;
#22737=ORIENTED_EDGE ( 'NONE', *, *, #11868, .T. ) ;
#22778=VERTEX_POINT ( 'NONE', #14846 ) ;
#22798=CARTESIAN_POINT ( 'NONE',  ( 12.70000000000017693, -3582.670000000000073, 2245.359999999999673 ) ) ;
#22833=FACE_OUTER_BOUND ( 'NONE', #14684, .T. ) ;
#22864=CARTESIAN_POINT ( 'NONE',  ( 12.69999999999999929, -3579.494999999999891, 2245.359999999999673 ) ) ;
#22869=EDGE_CURVE ( 'NONE', #10958, #3857, #4451, .T. ) ;
#22885=EDGE_CURVE ( 'NONE', #6235, #13538, #2578, .T. ) ;
#22926=DIRECTION ( 'NONE',  ( 0.8660254037820785955, -0.5000000000040877302, -3.181634500919918361E-14 ) ) ;
#22947=ORIENTED_EDGE ( 'NONE', *, *, #11173, .F. ) ;
#22967=( BOUNDED_CURVE ( )  B_SPLINE_CURVE ( 3, ( #16590, #7234, #17157, #991 ),
 .UNSPECIFIED., .F., .F. ) 
 B_SPLINE_CURVE_WITH_KNOTS ( ( 4, 4 ),
 ( 1.570796327146205540, 3.141592653589829531 ),
 .UNSPECIFIED. ) 
 CURVE ( )  GEOMETRIC_REPRESENTATION_ITEM ( )  RATIONAL_B_SPLINE_CURVE ( ( 1.000000000000000000, 0.8047378542071605967, 0.8047378542071605967, 1.000000000000000000 ) ) 
 REPRESENTATION_ITEM ( '' )  );
#23003=EDGE_CURVE ( 'NONE', #15456, #22532, #17271, .T. ) ;
#23026=FACE_OUTER_BOUND ( 'NONE', #12128, .T. ) ;
#23027=AXIS2_PLACEMENT_3D ( 'NONE', #22360, #7968, #13703 ) ;
#23057=CARTESIAN_POINT ( 'NONE',  ( 10.21049783553369217, -3580.932314744964970, 2239.009999999927913 ) ) ;
#23061=VERTEX_POINT ( 'NONE', #172 ) ;
#23068=CARTESIAN_POINT ( 'NONE',  ( 15.41268679717000012, -3579.494999999999891, 2239.391000000000076 ) ) ;
#23080=DIRECTION ( 'NONE',  ( -1.000000000000000000, 0.000000000000000000, 0.000000000000000000 ) ) ;
#23083=DIRECTION ( 'NONE',  ( 0.000000000000000000, -1.000000000000000000, 0.000000000000000000 ) ) ;
#23094=( NAMED_UNIT ( * ) SI_UNIT ( $, .STERADIAN. ) SOLID_ANGLE_UNIT ( ) );
#23104=ADVANCED_FACE ( 'NONE', ( #3681 ), #6357, .T. ) ;
#23208=COLOUR_RGB('Black',0.12,0.14,0.17);
#23209=FILL_AREA_STYLE_COLOUR('',#23208);
#23210=FILL_AREA_STYLE('',(#23209));
#23211=SURFACE_STYLE_FILL_AREA(#23210);
#23212=SURFACE_SIDE_STYLE('',(#23211));
#23213=SURFACE_STYLE_USAGE(.BOTH.,#23212);
#23214=PRESENTATION_STYLE_ASSIGNMENT((#23213));
#23228=STYLED_ITEM('',(#23214),#13990);
#23237=MECHANICAL_DESIGN_GEOMETRIC_PRESENTATION_REPRESENTATION('',(#23228),#2257);
ENDSEC;
END-ISO-10303-21;
